ISO-10303-21;
HEADER;
/* Generated by software containing ST-Developer
 * from STEP Tools, Inc. (www.steptools.com) 
 */

FILE_DESCRIPTION(
/* description */ ('Belt tensioner idler arm'),
/* implementation_level */ '2;1');

FILE_NAME(
/* name */ 'M3 pulley set screw.step',
/* time_stamp */ '2026-10-28T03:22:15-07:00',
/* author */ (''),
/* organization */ (''),
/* preprocessor_version */ 'ST-DEVELOPER v20.2',
/* originating_system */ 'Autodesk Translation Framework v15.17.0.0',
/* authorisation */ '');

FILE_SCHEMA (('AUTOMOTIVE_DESIGN { 1 0 10303 214 3 1 1 }'));
ENDSEC;

DATA;
#10=MECHANICAL_DESIGN_GEOMETRIC_PRESENTATION_REPRESENTATION('',(#483),#12779);
#407=SHAPE_REPRESENTATION_RELATIONSHIP('SRR','None',#12956,#441);
#441=ADVANCED_BREP_SHAPE_REPRESENTATION('',(#522),#12773);
#483=STYLED_ITEM('',(#13191),#522);
#522=MANIFOLD_SOLID_BREP('Body1',#6220);
#806=PLANE('',#7203);
#807=PLANE('',#7204);
#1114=FACE_OUTER_BOUND('',#1602,.T.);
#1115=FACE_OUTER_BOUND('',#1603,.T.);
#1116=FACE_OUTER_BOUND('',#1604,.T.);
#1602=EDGE_LOOP('',(#5212,#5213,#5214,#5215));
#1603=EDGE_LOOP('',(#5216));
#1604=EDGE_LOOP('',(#5217));
#1959=LINE('',#11922,#2308);
#2308=VECTOR('',#8885,0.15);
#2663=CIRCLE('',#7201,0.15);
#2664=CIRCLE('',#7202,0.15);
#3146=VERTEX_POINT('',#11919);
#3147=VERTEX_POINT('',#11921);
#3861=EDGE_CURVE('',#3146,#3146,#2663,.T.);
#3862=EDGE_CURVE('',#3146,#3147,#1959,.T.);
#3863=EDGE_CURVE('',#3147,#3147,#2664,.T.);
#5212=ORIENTED_EDGE('',*,*,#3861,.F.);
#5213=ORIENTED_EDGE('',*,*,#3862,.T.);
#5214=ORIENTED_EDGE('',*,*,#3863,.T.);
#5215=ORIENTED_EDGE('',*,*,#3862,.F.);
#5216=ORIENTED_EDGE('',*,*,#3861,.T.);
#5217=ORIENTED_EDGE('',*,*,#3863,.F.);
#5759=CYLINDRICAL_SURFACE('',#7200,0.15);
#6091=ADVANCED_FACE('',(#1114),#5759,.T.);
#6092=ADVANCED_FACE('',(#1115),#806,.T.);
#6093=ADVANCED_FACE('',(#1116),#807,.F.);
#6220=CLOSED_SHELL('',(#6091,#6092,#6093));
#7199=AXIS2_PLACEMENT_3D('',#11917,#8879,#8880);
#7200=AXIS2_PLACEMENT_3D('',#11918,#8881,#8882);
#7201=AXIS2_PLACEMENT_3D('',#11920,#8883,#8884);
#7202=AXIS2_PLACEMENT_3D('',#11923,#8886,#8887);
#7203=AXIS2_PLACEMENT_3D('',#11924,#8888,#8889);
#7204=AXIS2_PLACEMENT_3D('',#11925,#8890,#8891);
#8879=DIRECTION('axis',(0.,0.,1.));
#8880=DIRECTION('refdir',(1.,0.,0.));
#8881=DIRECTION('center_axis',(1.,0.,0.));
#8882=DIRECTION('ref_axis',(0.,0.,-1.));
#8883=DIRECTION('center_axis',(1.,0.,0.));
#8884=DIRECTION('ref_axis',(0.,0.,-1.));
#8885=DIRECTION('',(-1.,0.,0.));
#8886=DIRECTION('center_axis',(1.,0.,0.));
#8887=DIRECTION('ref_axis',(0.,0.,-1.));
#8888=DIRECTION('center_axis',(1.,0.,0.));
#8889=DIRECTION('ref_axis',(0.,0.,-1.));
#8890=DIRECTION('center_axis',(1.,0.,0.));
#8891=DIRECTION('ref_axis',(0.,0.,-1.));
#11917=CARTESIAN_POINT('',(0.,0.,0.));
#11918=CARTESIAN_POINT('Origin',(8.35,0.,7.55));
#11919=CARTESIAN_POINT('',(8.6,-1.83697019872103E-17,7.7));
#11920=CARTESIAN_POINT('Origin',(8.6,0.,7.55));
#11921=CARTESIAN_POINT('',(8.35,-1.83697019872103E-17,7.7));
#11922=CARTESIAN_POINT('',(8.35,-1.83697019872103E-17,7.7));
#11923=CARTESIAN_POINT('Origin',(8.35,0.,7.55));
#11924=CARTESIAN_POINT('Origin',(8.6,0.,7.55));
#11925=CARTESIAN_POINT('Origin',(8.35,0.,7.55));
#12733=UNCERTAINTY_MEASURE_WITH_UNIT(LENGTH_MEASURE(0.001),#12780,
'DISTANCE_ACCURACY_VALUE',
'Maximum model space distance between geometric entities at asserted c
onnectivities');
#12739=UNCERTAINTY_MEASURE_WITH_UNIT(LENGTH_MEASURE(0.001),#12780,
'DISTANCE_ACCURACY_VALUE',
'Maximum model space distance between geometric entities at asserted c
onnectivities');
#12773=(
GEOMETRIC_REPRESENTATION_CONTEXT(3)
GLOBAL_UNCERTAINTY_ASSIGNED_CONTEXT((#12733))
GLOBAL_UNIT_ASSIGNED_CONTEXT((#12780,#12782,#12783))
REPRESENTATION_CONTEXT('','3D')
);
#12779=(
GEOMETRIC_REPRESENTATION_CONTEXT(3)
GLOBAL_UNCERTAINTY_ASSIGNED_CONTEXT((#12739))
GLOBAL_UNIT_ASSIGNED_CONTEXT((#12780,#12782,#12783))
REPRESENTATION_CONTEXT('','3D')
);
#12780=(
LENGTH_UNIT()
NAMED_UNIT(*)
SI_UNIT(.CENTI.,.METRE.)
);
#12782=(
NAMED_UNIT(*)
PLANE_ANGLE_UNIT()
SI_UNIT($,.RADIAN.)
);
#12783=(
NAMED_UNIT(*)
SI_UNIT($,.STERADIAN.)
SOLID_ANGLE_UNIT()
);
#12817=SHAPE_DEFINITION_REPRESENTATION(#12885,#12956);
#12885=PRODUCT_DEFINITION_SHAPE('',$,#12996);
#12956=SHAPE_REPRESENTATION('',(#7199),#12773);
#12962=PRODUCT_DEFINITION_CONTEXT('part definition',#13081,'design');
#12996=PRODUCT_DEFINITION('M3 pulley set screw','M3 pulley set screw',#13035,
#12962);
#13035=PRODUCT_DEFINITION_FORMATION('',$,#13116);
#13081=APPLICATION_CONTEXT(
'Core Data for Automotive Mechanical Design Process');
#13082=PRODUCT_CONTEXT('part definition',#13081,'mechanical');
#13116=PRODUCT('M3 pulley set screw','M3 pulley set screw',
'M3 pulley set screw',(#13082));
#13185=COLOUR_RGB('Black',0.12,0.14,0.17);
#13186=FILL_AREA_STYLE_COLOUR('',#13185);
#13187=FILL_AREA_STYLE('',(#13186));
#13188=SURFACE_STYLE_FILL_AREA(#13187);
#13189=SURFACE_SIDE_STYLE('',(#13188));
#13190=SURFACE_STYLE_USAGE(.BOTH.,#13189);
#13191=PRESENTATION_STYLE_ASSIGNMENT((#13190));
ENDSEC;
END-ISO-10303-21;
